ISO-10303-21;
HEADER;
FILE_DESCRIPTION (('STEP AP214'),
    '1' );
FILE_NAME ('Central Pivot.step',
    '2026-09-24T10:15:42',
    ( '' ),
    ( '' ),
    'SwSTEP 2.0',
    'SolidWorks 2026',
    '' );
FILE_SCHEMA (( 'AUTOMOTIVE_DESIGN' ));
ENDSEC;

DATA;
#39=CARTESIAN_POINT ( 'NONE',  ( -30.00000000000000355, -12.50000000000000178, 6.000000000000000000 ) ) ;
#72=DIRECTION ( 'NONE',  ( 0.000000000000000000, 0.000000000000000000, -1.000000000000000000 ) ) ;
#101=EDGE_LOOP ( 'NONE', ( #9745, #3721, #17119, #3516 ) ) ;
#215=ADVANCED_FACE ( 'NONE', ( #233 ), #4532, .T. ) ;
#233=FACE_OUTER_BOUND ( 'NONE', #2264, .T. ) ;
#329=ORIENTED_EDGE ( 'NONE', *, *, #13463, .T. ) ;
#347=VERTEX_POINT ( 'NONE', #9760 ) ;
#380=DIRECTION ( 'NONE',  ( 0.000000000000000000, 0.000000000000000000, -1.000000000000000000 ) ) ;
#442=AXIS2_PLACEMENT_3D ( 'NONE', #9810, #18422, #11362 ) ;
#461=CIRCLE ( 'NONE', #9310, 0.5000000000000004441 ) ;
#476=CIRCLE ( 'NONE', #16019, 3.499999999999992895 ) ;
#486=DIRECTION ( 'NONE',  ( 0.000000000000000000, 0.000000000000000000, -1.000000000000000000 ) ) ;
#501=CIRCLE ( 'NONE', #2610, 2.499999999999995115 ) ;
#532=CARTESIAN_POINT ( 'NONE',  ( -33.49999999999999289, -12.50000000000000178, 7.000000000000000000 ) ) ;
#536=AXIS2_PLACEMENT_3D ( 'NONE', #4234, #16950, #9684 ) ;
#575=FACE_OUTER_BOUND ( 'NONE', #17278, .T. ) ;
#606=CIRCLE ( 'NONE', #10991, 0.5000000000000004441 ) ;
#693=VECTOR ( 'NONE', #8023, 1000.000000000000000 ) ;
#707=CARTESIAN_POINT ( 'NONE',  ( -33.99999999999999289, -12.50000000000000178, -0.5000000000000000000 ) ) ;
#716=SURFACE_STYLE_FILL_AREA ( #10759 ) ;
#727=AXIS2_PLACEMENT_3D ( 'NONE', #3087, #13233, #10571 ) ;
#762=CARTESIAN_POINT ( 'NONE',  ( -30.00000000000000355, -12.50000000000000178, 6.500000000000000888 ) ) ;
#811=SURFACE_STYLE_USAGE ( .BOTH. , #17931 ) ;
#899=AXIS2_PLACEMENT_3D ( 'NONE', #17631, #10363, #9124 ) ;
#910=ORIENTED_EDGE ( 'NONE', *, *, #9287, .F. ) ;
#1066=( NAMED_UNIT ( * ) SI_UNIT ( $, .STERADIAN. ) SOLID_ANGLE_UNIT ( ) );
#1086=ORIENTED_EDGE ( 'NONE', *, *, #10179, .T. ) ;
#1114=AXIS2_PLACEMENT_3D ( 'NONE', #3088, #8932, #9328 ) ;
#1139=CARTESIAN_POINT ( 'NONE',  ( -30.00000000000000355, -12.50000000000000178, -0.5000000000000000000 ) ) ;
#1213=ADVANCED_FACE ( 'NONE', ( #18685 ), #14306, .T. ) ;
#1215=FACE_OUTER_BOUND ( 'NONE', #8044, .T. ) ;
#1323=EDGE_LOOP ( 'NONE', ( #2426, #4863, #8855, #15183 ) ) ;
#1378=DIRECTION ( 'NONE',  ( 1.000000000000000000, 0.000000000000000000, 0.000000000000000000 ) ) ;
#1394=CIRCLE ( 'NONE', #16957, 3.499999999999992895 ) ;
#1475=ORIENTED_EDGE ( 'NONE', *, *, #9024, .T. ) ;
#1674=CIRCLE ( 'NONE', #2565, 3.499999999999992895 ) ;
#1690=CARTESIAN_POINT ( 'NONE',  ( -30.00000000000000355, -12.50000000000000178, -7.071067811865460406 ) ) ;
#1732=CIRCLE ( 'NONE', #14545, 0.5000000000000004441 ) ;
#1747=CLOSED_SHELL ( 'NONE', ( #3095, #17796, #12636, #7500, #4544, #6621, #1213, #10594, #18722, #17795, #18340, #215, #6090, #6941 ) ) ;
#1795=CARTESIAN_POINT ( 'NONE',  ( -33.99999999999999289, -12.50000000000000178, 6.500000000000000888 ) ) ;
#1818=DIRECTION ( 'NONE',  ( -0.000000000000000000, -0.000000000000000000, 1.000000000000000000 ) ) ;
#1898=CARTESIAN_POINT ( 'NONE',  ( -33.49999999999999289, -12.50000000000000178, -0.5000000000000000000 ) ) ;
#2004=TOROIDAL_SURFACE ( 'NONE', #8710, 3.499999999999994671, 0.5000000000000000000 ) ;
#2030=AXIS2_PLACEMENT_3D ( 'NONE', #15716, #11248, #17249 ) ;
#2060=DIRECTION ( 'NONE',  ( -1.224646799147353207E-16, 1.000000000000000000, 0.000000000000000000 ) ) ;
#2150=CARTESIAN_POINT ( 'NONE',  ( -30.00000000000000355, -12.50000000000000178, 0.000000000000000000 ) ) ;
#2234=DIRECTION ( 'NONE',  ( -1.000000000000000000, 0.000000000000000000, 0.000000000000000000 ) ) ;
#2264=EDGE_LOOP ( 'NONE', ( #18575, #7025, #6329, #18141 ) ) ;
#2285=AXIS2_PLACEMENT_3D ( 'NONE', #15810, #3878, #15712 ) ;
#2300=CIRCLE ( 'NONE', #14190, 3.499999999999992895 ) ;
#2321=FILL_AREA_STYLE ('',( #17216 ) ) ;
#2323=DIRECTION ( 'NONE',  ( -0.000000000000000000, -0.000000000000000000, 1.000000000000000000 ) ) ;
#2326=AXIS2_PLACEMENT_3D ( 'NONE', #16421, #13245, #6285 ) ;
#2337=VERTEX_POINT ( 'NONE', #5989 ) ;
#2385=DIRECTION ( 'NONE',  ( -1.000000000000000000, 0.000000000000000000, 0.000000000000000000 ) ) ;
#2426=ORIENTED_EDGE ( 'NONE', *, *, #3537, .F. ) ;
#2461=DIRECTION ( 'NONE',  ( 0.000000000000000000, 0.000000000000000000, 1.000000000000000000 ) ) ;
#2516=DIRECTION ( 'NONE',  ( 1.000000000000000000, 0.000000000000000000, 0.000000000000000000 ) ) ;
#2534=CARTESIAN_POINT ( 'NONE',  ( -30.00000000000000355, -12.50000000000000178, -0.5000000000000000000 ) ) ;
#2565=AXIS2_PLACEMENT_3D ( 'NONE', #15567, #14134, #2743 ) ;
#2583=ADVANCED_BREP_SHAPE_REPRESENTATION ( '', ( #3619, #2030 ), #8722 ) ;
#2602=DIRECTION ( 'NONE',  ( 1.000000000000000000, 0.000000000000000000, 0.000000000000000000 ) ) ;
#2610=AXIS2_PLACEMENT_3D ( 'NONE', #39, #18864, #1378 ) ;
#2643=PLANE ( 'NONE',  #442 ) ;
#2661=AXIS2_PLACEMENT_3D ( 'NONE', #4448, #14665, #10468 ) ;
#2700=CARTESIAN_POINT ( 'NONE',  ( -27.50000000000000711, -12.50000000000000178, -7.071067811865460406 ) ) ;
#2706=EDGE_CURVE ( 'NONE', #347, #18407, #1732, .T. ) ;
#2707=FACE_OUTER_BOUND ( 'NONE', #10285, .T. ) ;
#2737=ORIENTED_EDGE ( 'NONE', *, *, #7089, .F. ) ;
#2743=DIRECTION ( 'NONE',  ( 1.000000000000000000, 0.000000000000000000, 0.000000000000000000 ) ) ;
#2819=AXIS2_PLACEMENT_3D ( 'NONE', #1898, #3692, #7831 ) ;
#2868=AXIS2_PLACEMENT_3D ( 'NONE', #8380, #8294, #14484 ) ;
#2900=CIRCLE ( 'NONE', #2326, 2.499999999999995115 ) ;
#2909=EDGE_CURVE ( 'NONE', #4576, #11470, #8755, .T. ) ;
#2917=DIRECTION ( 'NONE',  ( 0.000000000000000000, -1.000000000000000000, 0.000000000000000000 ) ) ;
#2924=ORIENTED_EDGE ( 'NONE', *, *, #15352, .F. ) ;
#2946=AXIS2_PLACEMENT_3D ( 'NONE', #8725, #14838, #11978 ) ;
#2965=CIRCLE ( 'NONE', #8473, 3.999999999999993339 ) ;
#3000=ORIENTED_EDGE ( 'NONE', *, *, #7475, .F. ) ;
#3018=ORIENTED_EDGE ( 'NONE', *, *, #7834, .F. ) ;
#3087=CARTESIAN_POINT ( 'NONE',  ( -33.49999999999999289, -12.50000000000000178, -0.5000000000000000000 ) ) ;
#3088=CARTESIAN_POINT ( 'NONE',  ( -30.00000000000000355, -12.50000000000000178, 6.000000000000000000 ) ) ;
#3095=ADVANCED_FACE ( 'NONE', ( #18420 ), #15464, .T. ) ;
#3223=LINE ( 'NONE', #9070, #4117 ) ;
#3238=ORIENTED_EDGE ( 'NONE', *, *, #17327, .F. ) ;
#3248=PRODUCT ( 'Central Pivot', 'Central Pivot', '', ( #3764 ) ) ;
#3303=CARTESIAN_POINT ( 'NONE',  ( -27.50000000000000711, -12.50000000000000178, 6.000000000000000000 ) ) ;
#3312=DIRECTION ( 'NONE',  ( -1.000000000000000000, 0.000000000000000000, 0.000000000000000000 ) ) ;
#3468=ORIENTED_EDGE ( 'NONE', *, *, #13628, .T. ) ;
#3483=( NAMED_UNIT ( * ) PLANE_ANGLE_UNIT ( ) SI_UNIT ( $, .RADIAN. ) );
#3516=ORIENTED_EDGE ( 'NONE', *, *, #13944, .F. ) ;
#3537=EDGE_CURVE ( 'NONE', #18407, #9529, #14631, .T. ) ;
#3544=CIRCLE ( 'NONE', #7836, 3.999999999999993339 ) ;
#3619=MANIFOLD_SOLID_BREP ( 'Fillet1', #1747 ) ;
#3692=DIRECTION ( 'NONE',  ( -0.000000000000000000, -1.000000000000000000, -0.000000000000000000 ) ) ;
#3721=ORIENTED_EDGE ( 'NONE', *, *, #3991, .T. ) ;
#3764=PRODUCT_CONTEXT ( 'NONE', #7049, 'mechanical' ) ;
#3878=DIRECTION ( 'NONE',  ( 0.000000000000000000, 0.000000000000000000, -1.000000000000000000 ) ) ;
#3991=EDGE_CURVE ( 'NONE', #14770, #13012, #606, .T. ) ;
#4069=CIRCLE ( 'NONE', #727, 0.5000000000000000000 ) ;
#4117=VECTOR ( 'NONE', #9256, 1000.000000000000000 ) ;
#4184=CIRCLE ( 'NONE', #1114, 3.499999999999992895 ) ;
#4187=FACE_OUTER_BOUND ( 'NONE', #17414, .T. ) ;
#4234=CARTESIAN_POINT ( 'NONE',  ( -30.00000000000000355, -12.50000000000000178, 0.000000000000000000 ) ) ;
#4246=CARTESIAN_POINT ( 'NONE',  ( -30.00000000000000355, -12.50000000000000178, 6.500000000000000888 ) ) ;
#4358=EDGE_LOOP ( 'NONE', ( #3000, #9279, #329, #5658 ) ) ;
#4365=ORIENTED_EDGE ( 'NONE', *, *, #8665, .F. ) ;
#4385=DIRECTION ( 'NONE',  ( -0.000000000000000000, -0.000000000000000000, 1.000000000000000000 ) ) ;
#4412=TOROIDAL_SURFACE ( 'NONE', #16003, 3.499999999999994671, 0.5000000000000000000 ) ;
#4448=CARTESIAN_POINT ( 'NONE',  ( -26.50000000000001066, -12.50000000000000178, 6.500000000000000888 ) ) ;
#4500=AXIS2_PLACEMENT_3D ( 'NONE', #4246, #8631, #2602 ) ;
#4532=TOROIDAL_SURFACE ( 'NONE', #6976, 3.499999999999994671, 0.5000000000000000000 ) ;
#4544=ADVANCED_FACE ( 'NONE', ( #4187 ), #10001, .T. ) ;
#4569=( GEOMETRIC_REPRESENTATION_CONTEXT ( 3 ) GLOBAL_UNCERTAINTY_ASSIGNED_CONTEXT ( ( #9768 ) ) GLOBAL_UNIT_ASSIGNED_CONTEXT ( ( #11310, #5280, #1066 ) ) REPRESENTATION_CONTEXT ( 'NONE', 'WORKASPACE' ) );
#4576=VERTEX_POINT ( 'NONE', #17663 ) ;
#4658=DIRECTION ( 'NONE',  ( 1.000000000000000000, 0.000000000000000000, 0.000000000000000000 ) ) ;
#4771=DIRECTION ( 'NONE',  ( 0.000000000000000000, 0.000000000000000000, -1.000000000000000000 ) ) ;
#4778=DIRECTION ( 'NONE',  ( -1.000000000000000000, 0.000000000000000000, 0.000000000000000000 ) ) ;
#4828=EDGE_CURVE ( 'NONE', #18407, #7261, #12630, .T. ) ;
#4863=ORIENTED_EDGE ( 'NONE', *, *, #8438, .F. ) ;
#5132=CARTESIAN_POINT ( 'NONE',  ( -30.00000000000000355, -12.50000000000000178, 0.000000000000000000 ) ) ;
#5266=DIRECTION ( 'NONE',  ( 0.000000000000000000, 0.000000000000000000, -1.000000000000000000 ) ) ;
#5280=( NAMED_UNIT ( * ) PLANE_ANGLE_UNIT ( ) SI_UNIT ( $, .RADIAN. ) );
#5469=STYLED_ITEM ( 'NONE', ( #6732 ), #3619 ) ;
#5484=FACE_OUTER_BOUND ( 'NONE', #16147, .T. ) ;
#5648=MECHANICAL_DESIGN_GEOMETRIC_PRESENTATION_REPRESENTATION('',(#13907),#18786);
#5658=ORIENTED_EDGE ( 'NONE', *, *, #10179, .F. ) ;
#5804=EDGE_LOOP ( 'NONE', ( #910, #13167, #15336, #6277 ) ) ;
#5881=ORIENTED_EDGE ( 'NONE', *, *, #7591, .F. ) ;
#5989=CARTESIAN_POINT ( 'NONE',  ( -33.49999999999999289, -12.50000000000000178, 0.000000000000000000 ) ) ;
#6061=DIRECTION ( 'NONE',  ( 0.000000000000000000, 0.000000000000000000, -1.000000000000000000 ) ) ;
#6090=ADVANCED_FACE ( 'NONE', ( #17329 ), #12729, .T. ) ;
#6094=EDGE_LOOP ( 'NONE', ( #3238, #10792 ) ) ;
#6199=DIRECTION ( 'NONE',  ( 0.000000000000000000, 0.000000000000000000, 1.000000000000000000 ) ) ;
#6277=ORIENTED_EDGE ( 'NONE', *, *, #12050, .F. ) ;
#6285=DIRECTION ( 'NONE',  ( 1.000000000000000000, 0.000000000000000000, 0.000000000000000000 ) ) ;
#6329=ORIENTED_EDGE ( 'NONE', *, *, #12050, .T. ) ;
#6367=DIRECTION ( 'NONE',  ( 0.000000000000000000, 0.000000000000000000, 1.000000000000000000 ) ) ;
#6441=CARTESIAN_POINT ( 'NONE',  ( -26.00000000000001066, -12.50000000000000178, 6.500000000000000888 ) ) ;
#6464=ORIENTED_EDGE ( 'NONE', *, *, #13463, .F. ) ;
#6492=DIRECTION ( 'NONE',  ( -1.000000000000000000, 0.000000000000000000, 0.000000000000000000 ) ) ;
#6531=ORIENTED_EDGE ( 'NONE', *, *, #8329, .F. ) ;
#6545=CIRCLE ( 'NONE', #16308, 3.999999999999993339 ) ;
#6549=SHAPE_DEFINITION_REPRESENTATION ( #10270, #8995 ) ;
#6593=CARTESIAN_POINT ( 'NONE',  ( -30.00000000000000355, -12.50000000000000178, 6.500000000000000888 ) ) ;
#6621=ADVANCED_FACE ( 'NONE', ( #17098 ), #9554, .T. ) ;
#6649=( NAMED_UNIT ( * ) SI_UNIT ( $, .STERADIAN. ) SOLID_ANGLE_UNIT ( ) );
#6706=FACE_OUTER_BOUND ( 'NONE', #11255, .T. ) ;
#6732=PRESENTATION_STYLE_ASSIGNMENT (( #6815 ) ) ;
#6815=SURFACE_STYLE_USAGE ( .BOTH. , #18466 ) ;
#6834=AXIS2_PLACEMENT_3D ( 'NONE', #1690, #11827, #4658 ) ;
#6941=ADVANCED_FACE ( 'NONE', ( #575 ), #15022, .T. ) ;
#6955=CIRCLE ( 'NONE', #2661, 0.5000000000000004441 ) ;
#6976=AXIS2_PLACEMENT_3D ( 'NONE', #7792, #6061, #17819 ) ;
#7025=ORIENTED_EDGE ( 'NONE', *, *, #13628, .F. ) ;
#7049=APPLICATION_CONTEXT ( 'automotive_design' ) ;
#7089=EDGE_CURVE ( 'NONE', #11470, #8138, #18322, .T. ) ;
#7254=DIRECTION ( 'NONE',  ( 0.000000000000000000, 0.000000000000000000, -1.000000000000000000 ) ) ;
#7261=VERTEX_POINT ( 'NONE', #707 ) ;
#7315=MECHANICAL_DESIGN_GEOMETRIC_PRESENTATION_REPRESENTATION('',(#5469),#4569);
#7349=PLANE ( 'NONE',  #13603 ) ;
#7475=EDGE_CURVE ( 'NONE', #13012, #16693, #461, .T. ) ;
#7500=ADVANCED_FACE ( 'NONE', ( #6706 ), #4412, .T. ) ;
#7591=EDGE_CURVE ( 'NONE', #7599, #14770, #1674, .T. ) ;
#7599=VERTEX_POINT ( 'NONE', #13955 ) ;
#7654=CARTESIAN_POINT ( 'NONE',  ( -30.00000000000000355, -12.50000000000000178, -1.000000000000000000 ) ) ;
#7711=SHAPE_REPRESENTATION_RELATIONSHIP ( 'NONE' , 'NONE' ,  #8995, #2583 ) ;
#7772=EDGE_CURVE ( 'NONE', #9529, #10646, #15703, .T. ) ;
#7792=CARTESIAN_POINT ( 'NONE',  ( -30.00000000000000355, -12.50000000000000178, -0.5000000000000000000 ) ) ;
#7805=DIRECTION ( 'NONE',  ( 1.000000000000000000, 0.000000000000000000, 0.000000000000000000 ) ) ;
#7831=DIRECTION ( 'NONE',  ( 0.000000000000000000, 0.000000000000000000, -1.000000000000000000 ) ) ;
#7834=EDGE_CURVE ( 'NONE', #4576, #12327, #3223, .T. ) ;
#7836=AXIS2_PLACEMENT_3D ( 'NONE', #2534, #10989, #11170 ) ;
#7974=ORIENTED_EDGE ( 'NONE', *, *, #2909, .T. ) ;
#7991=DIRECTION ( 'NONE',  ( -1.000000000000000000, 0.000000000000000000, 0.000000000000000000 ) ) ;
#8023=DIRECTION ( 'NONE',  ( 0.000000000000000000, 0.000000000000000000, 1.000000000000000000 ) ) ;
#8044=EDGE_LOOP ( 'NONE', ( #14655, #12180 ) ) ;
#8138=VERTEX_POINT ( 'NONE', #3303 ) ;
#8219=CARTESIAN_POINT ( 'NONE',  ( -26.00000000000001066, -12.50000000000000178, -0.5000000000000000000 ) ) ;
#8253=EDGE_LOOP ( 'NONE', ( #15771, #1475 ) ) ;
#8285=CARTESIAN_POINT ( 'NONE',  ( -30.00000000000000355, -12.50000000000000178, 6.500000000000000888 ) ) ;
#8294=DIRECTION ( 'NONE',  ( 0.000000000000000000, 0.000000000000000000, 1.000000000000000000 ) ) ;
#8329=EDGE_CURVE ( 'NONE', #10646, #9529, #476, .T. ) ;
#8380=CARTESIAN_POINT ( 'NONE',  ( -30.00000000000000355, -12.50000000000000178, 7.000000000000000000 ) ) ;
#8390=DIRECTION ( 'NONE',  ( 1.000000000000000000, 0.000000000000000000, 0.000000000000000000 ) ) ;
#8403=CARTESIAN_POINT ( 'NONE',  ( -30.00000000000000355, -12.50000000000000178, -7.071067811865460406 ) ) ;
#8423=COLOUR_RGB ( '', 0.31764706, 0.68627451, 0.89019608) ;
#8438=EDGE_CURVE ( 'NONE', #7261, #18407, #3544, .T. ) ;
#8473=AXIS2_PLACEMENT_3D ( 'NONE', #8285, #18494, #17250 ) ;
#8480=ORIENTED_EDGE ( 'NONE', *, *, #10490, .F. ) ;
#8515=DIRECTION ( 'NONE',  ( -1.000000000000000000, 0.000000000000000000, 0.000000000000000000 ) ) ;
#8631=DIRECTION ( 'NONE',  ( 0.000000000000000000, 0.000000000000000000, 1.000000000000000000 ) ) ;
#8665=EDGE_CURVE ( 'NONE', #8138, #12327, #2900, .T. ) ;
#8710=AXIS2_PLACEMENT_3D ( 'NONE', #13565, #486, #13277 ) ;
#8722=( GEOMETRIC_REPRESENTATION_CONTEXT ( 3 ) GLOBAL_UNCERTAINTY_ASSIGNED_CONTEXT ( ( #17601 ) ) GLOBAL_UNIT_ASSIGNED_CONTEXT ( ( #13891, #16682, #6649 ) ) REPRESENTATION_CONTEXT ( 'NONE', 'WORKASPACE' ) );
#8725=CARTESIAN_POINT ( 'NONE',  ( -30.00000000000000355, -12.50000000000000178, 7.000000000000000000 ) ) ;
#8755=CIRCLE ( 'NONE', #536, 2.499999999999992006 ) ;
#8828=AXIS2_PLACEMENT_3D ( 'NONE', #14997, #1818, #4778 ) ;
#8855=ORIENTED_EDGE ( 'NONE', *, *, #10809, .T. ) ;
#8861=DIRECTION ( 'NONE',  ( -1.000000000000000000, 0.000000000000000000, -0.000000000000000000 ) ) ;
#8894=CARTESIAN_POINT ( 'NONE',  ( -33.49999999999999289, -12.50000000000000178, 6.500000000000000888 ) ) ;
#8932=DIRECTION ( 'NONE',  ( -0.000000000000000000, -0.000000000000000000, -1.000000000000000000 ) ) ;
#8995=SHAPE_REPRESENTATION ( 'Central Pivot', ( #2030 ), #8722 ) ;
#9024=EDGE_CURVE ( 'NONE', #12327, #8138, #501, .T. ) ;
#9070=CARTESIAN_POINT ( 'NONE',  ( -32.49999999999999289, -12.50000000000000178, -7.071067811865460406 ) ) ;
#9124=DIRECTION ( 'NONE',  ( -1.000000000000000000, 0.000000000000000000, 0.000000000000000000 ) ) ;
#9256=DIRECTION ( 'NONE',  ( 0.000000000000000000, 0.000000000000000000, 1.000000000000000000 ) ) ;
#9279=ORIENTED_EDGE ( 'NONE', *, *, #13726, .F. ) ;
#9287=EDGE_CURVE ( 'NONE', #347, #2337, #2300, .T. ) ;
#9310=AXIS2_PLACEMENT_3D ( 'NONE', #8894, #17603, #16268 ) ;
#9328=DIRECTION ( 'NONE',  ( 1.000000000000000000, 0.000000000000000000, 0.000000000000000000 ) ) ;
#9513=ORIENTED_EDGE ( 'NONE', *, *, #7089, .T. ) ;
#9529=VERTEX_POINT ( 'NONE', #18355 ) ;
#9554=CYLINDRICAL_SURFACE ( 'NONE', #16852, 2.499999999999995115 ) ;
#9570=ORIENTED_EDGE ( 'NONE', *, *, #10809, .F. ) ;
#9684=DIRECTION ( 'NONE',  ( -1.000000000000000000, 0.000000000000000000, 0.000000000000000000 ) ) ;
#9738=DIRECTION ( 'NONE',  ( 1.000000000000000000, 0.000000000000000000, 0.000000000000000000 ) ) ;
#9745=ORIENTED_EDGE ( 'NONE', *, *, #15026, .F. ) ;
#9760=CARTESIAN_POINT ( 'NONE',  ( -26.50000000000000711, -12.50000000000000178, 0.000000000000000000 ) ) ;
#9768=UNCERTAINTY_MEASURE_WITH_UNIT (LENGTH_MEASURE( 1.000000000000000082E-05 ), #11310, 'distance_accuracy_value', 'NONE');
#9810=CARTESIAN_POINT ( 'NONE',  ( -30.00000000000000355, -12.50000000000000178, 6.000000000000000000 ) ) ;
#9880=PLANE ( 'NONE',  #2285 ) ;
#10001=CYLINDRICAL_SURFACE ( 'NONE', #6834, 2.499999999999995115 ) ;
#10006=CARTESIAN_POINT ( 'NONE',  ( -33.49999999999999289, -12.50000000000000178, -1.000000000000000000 ) ) ;
#10088=EDGE_LOOP ( 'NONE', ( #17084, #1086 ) ) ;
#10114=TOROIDAL_SURFACE ( 'NONE', #12851, 3.499999999999994671, 0.5000000000000000000 ) ;
#10179=EDGE_CURVE ( 'NONE', #16693, #10980, #1394, .T. ) ;
#10198=CARTESIAN_POINT ( 'NONE',  ( -30.00000000000000355, -12.50000000000000178, -1.000000000000000000 ) ) ;
#10270=PRODUCT_DEFINITION_SHAPE ( 'NONE', 'NONE',  #12687 ) ;
#10285=EDGE_LOOP ( 'NONE', ( #8480, #11971, #2924, #6464 ) ) ;
#10333=ORIENTED_EDGE ( 'NONE', *, *, #7772, .T. ) ;
#10363=DIRECTION ( 'NONE',  ( -1.224646799147353207E-16, 1.000000000000000000, 0.000000000000000000 ) ) ;
#10468=DIRECTION ( 'NONE',  ( 0.000000000000000000, 0.000000000000000000, -1.000000000000000000 ) ) ;
#10490=EDGE_CURVE ( 'NONE', #13012, #16462, #6545, .T. ) ;
#10494=CARTESIAN_POINT ( 'NONE',  ( -26.50000000000001066, -12.50000000000000178, 6.500000000000000888 ) ) ;
#10508=PRODUCT_DEFINITION_FORMATION_WITH_SPECIFIED_SOURCE ( 'ANY', '', #3248, .NOT_KNOWN. ) ;
#10536=TOROIDAL_SURFACE ( 'NONE', #11442, 3.499999999999992450, 0.5000000000000000000 ) ;
#10571=DIRECTION ( 'NONE',  ( 0.000000000000000000, 0.000000000000000000, -1.000000000000000000 ) ) ;
#10591=FACE_OUTER_BOUND ( 'NONE', #16848, .T. ) ;
#10594=ADVANCED_FACE ( 'NONE', ( #1215, #12690 ), #2643, .F. ) ;
#10646=VERTEX_POINT ( 'NONE', #10006 ) ;
#10665=CARTESIAN_POINT ( 'NONE',  ( -30.00000000000000355, -12.50000000000000178, 7.000000000000000000 ) ) ;
#10759=FILL_AREA_STYLE ('',( #13517 ) ) ;
#10792=ORIENTED_EDGE ( 'NONE', *, *, #2909, .F. ) ;
#10809=EDGE_CURVE ( 'NONE', #7261, #10646, #15353, .T. ) ;
#10856=( LENGTH_UNIT ( ) NAMED_UNIT ( * ) SI_UNIT ( .MILLI., .METRE. ) );
#10907=DIRECTION ( 'NONE',  ( -0.000000000000000000, -0.000000000000000000, -1.000000000000000000 ) ) ;
#10980=VERTEX_POINT ( 'NONE', #18493 ) ;
#10989=DIRECTION ( 'NONE',  ( -0.000000000000000000, -0.000000000000000000, 1.000000000000000000 ) ) ;
#10991=AXIS2_PLACEMENT_3D ( 'NONE', #12339, #12520, #15484 ) ;
#11170=DIRECTION ( 'NONE',  ( -1.000000000000000000, 0.000000000000000000, 0.000000000000000000 ) ) ;
#11246=DIRECTION ( 'NONE',  ( 0.000000000000000000, 0.000000000000000000, 1.000000000000000000 ) ) ;
#11248=DIRECTION ( 'NONE',  ( 0.000000000000000000, 0.000000000000000000, 1.000000000000000000 ) ) ;
#11255=EDGE_LOOP ( 'NONE', ( #13377, #12289, #6531, #9570 ) ) ;
#11310=( LENGTH_UNIT ( ) NAMED_UNIT ( * ) SI_UNIT ( .MILLI., .METRE. ) );
#11362=DIRECTION ( 'NONE',  ( 1.000000000000000000, 0.000000000000000000, -0.000000000000000000 ) ) ;
#11375=DIRECTION ( 'NONE',  ( -1.000000000000000000, 0.000000000000000000, 0.000000000000000000 ) ) ;
#11442=AXIS2_PLACEMENT_3D ( 'NONE', #17151, #11246, #2516 ) ;
#11470=VERTEX_POINT ( 'NONE', #11877 ) ;
#11489=ORIENTED_EDGE ( 'NONE', *, *, #7834, .T. ) ;
#11509=ORIENTED_EDGE ( 'NONE', *, *, #13726, .T. ) ;
#11827=DIRECTION ( 'NONE',  ( 0.000000000000000000, 0.000000000000000000, 1.000000000000000000 ) ) ;
#11877=CARTESIAN_POINT ( 'NONE',  ( -27.50000000000000711, -12.50000000000000178, 0.000000000000000000 ) ) ;
#11971=ORIENTED_EDGE ( 'NONE', *, *, #7475, .T. ) ;
#11978=DIRECTION ( 'NONE',  ( 1.000000000000000000, 0.000000000000000000, 0.000000000000000000 ) ) ;
#12050=EDGE_CURVE ( 'NONE', #2337, #7261, #4069, .T. ) ;
#12180=ORIENTED_EDGE ( 'NONE', *, *, #15026, .T. ) ;
#12289=ORIENTED_EDGE ( 'NONE', *, *, #3537, .T. ) ;
#12327=VERTEX_POINT ( 'NONE', #17135 ) ;
#12339=CARTESIAN_POINT ( 'NONE',  ( -33.49999999999999289, -12.50000000000000178, 6.500000000000000888 ) ) ;
#12372=PRESENTATION_STYLE_ASSIGNMENT (( #811 ) ) ;
#12439=CIRCLE ( 'NONE', #2946, 3.499999999999992895 ) ;
#12520=DIRECTION ( 'NONE',  ( 1.224646799147353207E-16, 1.000000000000000000, -0.000000000000000000 ) ) ;
#12630=CIRCLE ( 'NONE', #14161, 3.999999999999993339 ) ;
#12636=ADVANCED_FACE ( 'NONE', ( #18274 ), #10114, .T. ) ;
#12670=CARTESIAN_POINT ( 'NONE',  ( -33.49999999999999289, -12.50000000000000178, 6.000000000000000000 ) ) ;
#12687=PRODUCT_DEFINITION ( 'UNKNOWN', '', #10508, #15169 ) ;
#12690=FACE_BOUND ( 'NONE', #8253, .T. ) ;
#12729=TOROIDAL_SURFACE ( 'NONE', #4500, 3.499999999999992450, 0.5000000000000000000 ) ;
#12820=SURFACE_STYLE_FILL_AREA ( #2321 ) ;
#12832=ORIENTED_EDGE ( 'NONE', *, *, #9287, .T. ) ;
#12838=AXIS2_PLACEMENT_3D ( 'NONE', #10494, #2917, #7254 ) ;
#12845=FACE_BOUND ( 'NONE', #6094, .T. ) ;
#12851=AXIS2_PLACEMENT_3D ( 'NONE', #15492, #5266, #8515 ) ;
#12859=ORIENTED_EDGE ( 'NONE', *, *, #3991, .F. ) ;
#12887=CARTESIAN_POINT ( 'NONE',  ( -30.00000000000000355, -12.50000000000000178, -0.5000000000000000000 ) ) ;
#13012=VERTEX_POINT ( 'NONE', #1795 ) ;
#13050=CIRCLE ( 'NONE', #18848, 3.499999999999992895 ) ;
#13070=ORIENTED_EDGE ( 'NONE', *, *, #9024, .F. ) ;
#13156=CIRCLE ( 'NONE', #12838, 0.5000000000000004441 ) ;
#13166=ORIENTED_EDGE ( 'NONE', *, *, #17327, .T. ) ;
#13167=ORIENTED_EDGE ( 'NONE', *, *, #2706, .T. ) ;
#13175=AXIS2_PLACEMENT_3D ( 'NONE', #13457, #6199, #17869 ) ;
#13233=DIRECTION ( 'NONE',  ( -0.000000000000000000, -1.000000000000000000, -0.000000000000000000 ) ) ;
#13245=DIRECTION ( 'NONE',  ( 0.000000000000000000, 0.000000000000000000, 1.000000000000000000 ) ) ;
#13277=DIRECTION ( 'NONE',  ( -1.000000000000000000, 0.000000000000000000, 0.000000000000000000 ) ) ;
#13377=ORIENTED_EDGE ( 'NONE', *, *, #4828, .F. ) ;
#13457=CARTESIAN_POINT ( 'NONE',  ( -30.00000000000000355, -12.50000000000000178, 6.500000000000000888 ) ) ;
#13463=EDGE_CURVE ( 'NONE', #16462, #10980, #13156, .T. ) ;
#13517=FILL_AREA_STYLE_COLOUR ( '', #8423 ) ;
#13565=CARTESIAN_POINT ( 'NONE',  ( -30.00000000000000355, -12.50000000000000178, -0.5000000000000000000 ) ) ;
#13603=AXIS2_PLACEMENT_3D ( 'NONE', #10198, #72, #8861 ) ;
#13605=EDGE_LOOP ( 'NONE', ( #3018, #7974, #9513, #13070 ) ) ;
#13628=EDGE_CURVE ( 'NONE', #2337, #347, #13050, .T. ) ;
#13726=EDGE_CURVE ( 'NONE', #16462, #13012, #2965, .T. ) ;
#13731=COLOUR_RGB ( '', 0.31764706, 0.68627451, 0.89019608) ;
#13752=DIRECTION ( 'NONE',  ( -1.000000000000000000, 0.000000000000000000, 0.000000000000000000 ) ) ;
#13891=( LENGTH_UNIT ( ) NAMED_UNIT ( * ) SI_UNIT ( .MILLI., .METRE. ) );
#13907=STYLED_ITEM ( 'NONE', ( #12372 ), #2583 ) ;
#13917=DIRECTION ( 'NONE',  ( -0.000000000000000000, -0.000000000000000000, 1.000000000000000000 ) ) ;
#13944=EDGE_CURVE ( 'NONE', #7599, #16462, #6955, .T. ) ;
#13955=CARTESIAN_POINT ( 'NONE',  ( -26.50000000000001066, -12.50000000000000178, 6.000000000000000000 ) ) ;
#14134=DIRECTION ( 'NONE',  ( -0.000000000000000000, -0.000000000000000000, -1.000000000000000000 ) ) ;
#14161=AXIS2_PLACEMENT_3D ( 'NONE', #12887, #4385, #11375 ) ;
#14190=AXIS2_PLACEMENT_3D ( 'NONE', #2150, #2323, #7991 ) ;
#14306=PLANE ( 'NONE',  #2868 ) ;
#14326=CIRCLE ( 'NONE', #8828, 2.499999999999992006 ) ;
#14484=DIRECTION ( 'NONE',  ( 1.000000000000000000, 0.000000000000000000, -0.000000000000000000 ) ) ;
#14485=APPLICATION_CONTEXT ( 'automotive_design' ) ;
#14545=AXIS2_PLACEMENT_3D ( 'NONE', #15146, #2060, #2234 ) ;
#14631=CIRCLE ( 'NONE', #899, 0.5000000000000004441 ) ;
#14655=ORIENTED_EDGE ( 'NONE', *, *, #7591, .T. ) ;
#14665=DIRECTION ( 'NONE',  ( 0.000000000000000000, -1.000000000000000000, 0.000000000000000000 ) ) ;
#14722=UNCERTAINTY_MEASURE_WITH_UNIT (LENGTH_MEASURE( 1.000000000000000082E-05 ), #10856, 'distance_accuracy_value', 'NONE');
#14770=VERTEX_POINT ( 'NONE', #12670 ) ;
#14838=DIRECTION ( 'NONE',  ( 0.000000000000000000, 0.000000000000000000, 1.000000000000000000 ) ) ;
#14992=CARTESIAN_POINT ( 'NONE',  ( -30.00000000000000355, -12.50000000000000178, -1.000000000000000000 ) ) ;
#14997=CARTESIAN_POINT ( 'NONE',  ( -30.00000000000000355, -12.50000000000000178, 0.000000000000000000 ) ) ;
#14999=FACE_OUTER_BOUND ( 'NONE', #1323, .T. ) ;
#15022=TOROIDAL_SURFACE ( 'NONE', #13175, 3.499999999999992450, 0.5000000000000000000 ) ;
#15026=EDGE_CURVE ( 'NONE', #14770, #7599, #4184, .T. ) ;
#15146=CARTESIAN_POINT ( 'NONE',  ( -26.50000000000000711, -12.50000000000000178, -0.5000000000000000000 ) ) ;
#15169=PRODUCT_DEFINITION_CONTEXT ( 'detailed design', #14485, 'design' ) ;
#15183=ORIENTED_EDGE ( 'NONE', *, *, #7772, .F. ) ;
#15336=ORIENTED_EDGE ( 'NONE', *, *, #4828, .T. ) ;
#15352=EDGE_CURVE ( 'NONE', #10980, #16693, #12439, .T. ) ;
#15353=CIRCLE ( 'NONE', #2819, 0.5000000000000000000 ) ;
#15464=TOROIDAL_SURFACE ( 'NONE', #17928, 3.499999999999992450, 0.5000000000000000000 ) ;
#15484=DIRECTION ( 'NONE',  ( -1.000000000000000000, 0.000000000000000000, 0.000000000000000000 ) ) ;
#15492=CARTESIAN_POINT ( 'NONE',  ( -30.00000000000000355, -12.50000000000000178, -0.5000000000000000000 ) ) ;
#15567=CARTESIAN_POINT ( 'NONE',  ( -30.00000000000000355, -12.50000000000000178, 6.000000000000000000 ) ) ;
#15703=CIRCLE ( 'NONE', #17540, 3.499999999999992895 ) ;
#15712=DIRECTION ( 'NONE',  ( -1.000000000000000000, 0.000000000000000000, -0.000000000000000000 ) ) ;
#15716=CARTESIAN_POINT ( 'NONE',  ( 0.000000000000000000, 0.000000000000000000, 0.000000000000000000 ) ) ;
#15771=ORIENTED_EDGE ( 'NONE', *, *, #8665, .T. ) ;
#15810=CARTESIAN_POINT ( 'NONE',  ( -30.00000000000000355, -12.50000000000000178, 0.000000000000000000 ) ) ;
#16003=AXIS2_PLACEMENT_3D ( 'NONE', #1139, #18350, #2385 ) ;
#16019=AXIS2_PLACEMENT_3D ( 'NONE', #14992, #380, #13752 ) ;
#16147=EDGE_LOOP ( 'NONE', ( #3468, #12832 ) ) ;
#16268=DIRECTION ( 'NONE',  ( -1.000000000000000000, 0.000000000000000000, 0.000000000000000000 ) ) ;
#16308=AXIS2_PLACEMENT_3D ( 'NONE', #762, #10907, #18335 ) ;
#16421=CARTESIAN_POINT ( 'NONE',  ( -30.00000000000000355, -12.50000000000000178, 6.000000000000000000 ) ) ;
#16462=VERTEX_POINT ( 'NONE', #6441 ) ;
#16663=ORIENTED_EDGE ( 'NONE', *, *, #8329, .T. ) ;
#16682=( NAMED_UNIT ( * ) PLANE_ANGLE_UNIT ( ) SI_UNIT ( $, .RADIAN. ) );
#16693=VERTEX_POINT ( 'NONE', #532 ) ;
#16848=EDGE_LOOP ( 'NONE', ( #16663, #10333 ) ) ;
#16852=AXIS2_PLACEMENT_3D ( 'NONE', #8403, #2461, #9738 ) ;
#16859=( NAMED_UNIT ( * ) SI_UNIT ( $, .STERADIAN. ) SOLID_ANGLE_UNIT ( ) );
#16950=DIRECTION ( 'NONE',  ( -0.000000000000000000, -0.000000000000000000, 1.000000000000000000 ) ) ;
#16957=AXIS2_PLACEMENT_3D ( 'NONE', #10665, #6367, #7805 ) ;
#17084=ORIENTED_EDGE ( 'NONE', *, *, #15352, .T. ) ;
#17098=FACE_OUTER_BOUND ( 'NONE', #13605, .T. ) ;
#17119=ORIENTED_EDGE ( 'NONE', *, *, #10490, .T. ) ;
#17135=CARTESIAN_POINT ( 'NONE',  ( -32.49999999999999289, -12.50000000000000178, 6.000000000000000000 ) ) ;
#17151=CARTESIAN_POINT ( 'NONE',  ( -30.00000000000000355, -12.50000000000000178, 6.500000000000000888 ) ) ;
#17216=FILL_AREA_STYLE_COLOUR ( '', #13731 ) ;
#17249=DIRECTION ( 'NONE',  ( 1.000000000000000000, 0.000000000000000000, 0.000000000000000000 ) ) ;
#17250=DIRECTION ( 'NONE',  ( 1.000000000000000000, 0.000000000000000000, 0.000000000000000000 ) ) ;
#17278=EDGE_LOOP ( 'NONE', ( #12859, #5881, #18319, #11509 ) ) ;
#17327=EDGE_CURVE ( 'NONE', #11470, #4576, #14326, .T. ) ;
#17329=FACE_OUTER_BOUND ( 'NONE', #4358, .T. ) ;
#17414=EDGE_LOOP ( 'NONE', ( #13166, #11489, #4365, #2737 ) ) ;
#17540=AXIS2_PLACEMENT_3D ( 'NONE', #7654, #4771, #6492 ) ;
#17601=UNCERTAINTY_MEASURE_WITH_UNIT (LENGTH_MEASURE( 1.000000000000000082E-05 ), #13891, 'distance_accuracy_value', 'NONE');
#17603=DIRECTION ( 'NONE',  ( 1.224646799147353207E-16, 1.000000000000000000, -0.000000000000000000 ) ) ;
#17631=CARTESIAN_POINT ( 'NONE',  ( -26.50000000000000711, -12.50000000000000178, -0.5000000000000000000 ) ) ;
#17663=CARTESIAN_POINT ( 'NONE',  ( -32.49999999999999289, -12.50000000000000178, 0.000000000000000000 ) ) ;
#17795=ADVANCED_FACE ( 'NONE', ( #5484, #12845 ), #9880, .F. ) ;
#17796=ADVANCED_FACE ( 'NONE', ( #2707 ), #10536, .T. ) ;
#17819=DIRECTION ( 'NONE',  ( -1.000000000000000000, 0.000000000000000000, 0.000000000000000000 ) ) ;
#17869=DIRECTION ( 'NONE',  ( 1.000000000000000000, 0.000000000000000000, 0.000000000000000000 ) ) ;
#17928=AXIS2_PLACEMENT_3D ( 'NONE', #6593, #18250, #8390 ) ;
#17931=SURFACE_SIDE_STYLE ('',( #716 ) ) ;
#18141=ORIENTED_EDGE ( 'NONE', *, *, #8438, .T. ) ;
#18250=DIRECTION ( 'NONE',  ( 0.000000000000000000, 0.000000000000000000, 1.000000000000000000 ) ) ;
#18274=FACE_OUTER_BOUND ( 'NONE', #5804, .T. ) ;
#18319=ORIENTED_EDGE ( 'NONE', *, *, #13944, .T. ) ;
#18322=LINE ( 'NONE', #2700, #693 ) ;
#18335=DIRECTION ( 'NONE',  ( 1.000000000000000000, 0.000000000000000000, 0.000000000000000000 ) ) ;
#18340=ADVANCED_FACE ( 'NONE', ( #14999 ), #2004, .T. ) ;
#18350=DIRECTION ( 'NONE',  ( 0.000000000000000000, 0.000000000000000000, -1.000000000000000000 ) ) ;
#18355=CARTESIAN_POINT ( 'NONE',  ( -26.50000000000000711, -12.50000000000000178, -1.000000000000000000 ) ) ;
#18407=VERTEX_POINT ( 'NONE', #8219 ) ;
#18420=FACE_OUTER_BOUND ( 'NONE', #101, .T. ) ;
#18422=DIRECTION ( 'NONE',  ( 0.000000000000000000, 0.000000000000000000, 1.000000000000000000 ) ) ;
#18466=SURFACE_SIDE_STYLE ('',( #12820 ) ) ;
#18493=CARTESIAN_POINT ( 'NONE',  ( -26.50000000000001066, -12.50000000000000178, 7.000000000000000000 ) ) ;
#18494=DIRECTION ( 'NONE',  ( -0.000000000000000000, -0.000000000000000000, -1.000000000000000000 ) ) ;
#18575=ORIENTED_EDGE ( 'NONE', *, *, #2706, .F. ) ;
#18685=FACE_OUTER_BOUND ( 'NONE', #10088, .T. ) ;
#18722=ADVANCED_FACE ( 'NONE', ( #10591 ), #7349, .T. ) ;
#18786=( GEOMETRIC_REPRESENTATION_CONTEXT ( 3 ) GLOBAL_UNCERTAINTY_ASSIGNED_CONTEXT ( ( #14722 ) ) GLOBAL_UNIT_ASSIGNED_CONTEXT ( ( #10856, #3483, #16859 ) ) REPRESENTATION_CONTEXT ( 'NONE', 'WORKASPACE' ) );
#18848=AXIS2_PLACEMENT_3D ( 'NONE', #5132, #13917, #3312 ) ;
#18864=DIRECTION ( 'NONE',  ( 0.000000000000000000, 0.000000000000000000, 1.000000000000000000 ) ) ;
ENDSEC;
END-ISO-10303-21;
